ISO-10303-21;
HEADER;
/* Generated by software containing ST-Developer
 * from STEP Tools, Inc. (www.steptools.com) 
 */

FILE_DESCRIPTION(
/* description */ (''),
/* implementation_level */ '2;1');

FILE_NAME(
/* name */ '10_Handle_Pin_D6x30.step',
/* time_stamp */ '2026-10-26T03:55:20-07:00',
/* author */ (''),
/* organization */ (''),
/* preprocessor_version */ 'ST-DEVELOPER v20.2',
/* originating_system */ 'Autodesk Translation Framework v15.15.0.0',
/* authorisation */ '');

FILE_SCHEMA (('AUTOMOTIVE_DESIGN { 1 0 10303 214 3 1 1 }'));
ENDSEC;

DATA;
#10=MECHANICAL_DESIGN_GEOMETRIC_PRESENTATION_REPRESENTATION('',(#192),#45236);
#152=SHAPE_REPRESENTATION_RELATIONSHIP('SRR','None',#45331,#172);
#172=ADVANCED_BREP_SHAPE_REPRESENTATION('',(#212),#45233);
#192=STYLED_ITEM('',(#45484),#212);
#212=MANIFOLD_SOLID_BREP('Body1',#16534);
#1055=FACE_BOUND('',#3846,.T.);
#1056=FACE_BOUND('',#3849,.T.);
#1057=FACE_BOUND('',#3852,.T.);
#1058=FACE_BOUND('',#3855,.T.);
#1541=PLANE('',#18029);
#1542=PLANE('',#18035);
#1543=PLANE('',#18039);
#1544=PLANE('',#18043);
#1545=PLANE('',#18047);
#1546=PLANE('',#18053);
#1805=CYLINDRICAL_SURFACE('',#18033,3.);
#1806=CYLINDRICAL_SURFACE('',#18037,2.5);
#1807=CYLINDRICAL_SURFACE('',#18041,3.);
#1808=CYLINDRICAL_SURFACE('',#18045,2.5);
#1809=CYLINDRICAL_SURFACE('',#18049,3.);
#2752=FACE_OUTER_BOUND('',#3842,.T.);
#2753=FACE_OUTER_BOUND('',#3843,.T.);
#2754=FACE_OUTER_BOUND('',#3844,.T.);
#2755=FACE_OUTER_BOUND('',#3845,.T.);
#2756=FACE_OUTER_BOUND('',#3847,.T.);
#2757=FACE_OUTER_BOUND('',#3848,.T.);
#2758=FACE_OUTER_BOUND('',#3850,.T.);
#2759=FACE_OUTER_BOUND('',#3851,.T.);
#2760=FACE_OUTER_BOUND('',#3853,.T.);
#2761=FACE_OUTER_BOUND('',#3854,.T.);
#2762=FACE_OUTER_BOUND('',#3856,.T.);
#2763=FACE_OUTER_BOUND('',#3857,.T.);
#2764=FACE_OUTER_BOUND('',#3858,.T.);
#3842=EDGE_LOOP('',(#15344));
#3843=EDGE_LOOP('',(#15345,#15346,#15347,#15348));
#3844=EDGE_LOOP('',(#15349,#15350,#15351,#15352));
#3845=EDGE_LOOP('',(#15353));
#3846=EDGE_LOOP('',(#15354));
#3847=EDGE_LOOP('',(#15355,#15356,#15357,#15358));
#3848=EDGE_LOOP('',(#15359));
#3849=EDGE_LOOP('',(#15360));
#3850=EDGE_LOOP('',(#15361,#15362,#15363,#15364));
#3851=EDGE_LOOP('',(#15365));
#3852=EDGE_LOOP('',(#15366));
#3853=EDGE_LOOP('',(#15367,#15368,#15369,#15370));
#3854=EDGE_LOOP('',(#15371));
#3855=EDGE_LOOP('',(#15372));
#3856=EDGE_LOOP('',(#15373,#15374,#15375,#15376));
#3857=EDGE_LOOP('',(#15377,#15378,#15379,#15380));
#3858=EDGE_LOOP('',(#15381));
#5159=LINE('',#45010,#6470);
#5160=LINE('',#45014,#6471);
#5161=LINE('',#45021,#6472);
#5162=LINE('',#45028,#6473);
#5163=LINE('',#45035,#6474);
#5164=LINE('',#45042,#6475);
#5165=LINE('',#45046,#6476);
#6470=VECTOR('',#21946,2.8);
#6471=VECTOR('',#21951,3.);
#6472=VECTOR('',#21960,2.5);
#6473=VECTOR('',#21969,3.);
#6474=VECTOR('',#21978,2.5);
#6475=VECTOR('',#21987,3.);
#6476=VECTOR('',#21992,2.8);
#6938=CIRCLE('',#18030,2.6);
#6939=CIRCLE('',#18032,3.);
#6940=CIRCLE('',#18034,3.);
#6941=CIRCLE('',#18036,2.5);
#6942=CIRCLE('',#18038,2.5);
#6943=CIRCLE('',#18040,3.);
#6944=CIRCLE('',#18042,3.);
#6945=CIRCLE('',#18044,2.5);
#6946=CIRCLE('',#18046,2.5);
#6947=CIRCLE('',#18048,3.);
#6948=CIRCLE('',#18050,3.);
#6949=CIRCLE('',#18052,2.6);
#8423=VERTEX_POINT('',#45005);
#8424=VERTEX_POINT('',#45008);
#8425=VERTEX_POINT('',#45012);
#8426=VERTEX_POINT('',#45016);
#8427=VERTEX_POINT('',#45019);
#8428=VERTEX_POINT('',#45023);
#8429=VERTEX_POINT('',#45026);
#8430=VERTEX_POINT('',#45030);
#8431=VERTEX_POINT('',#45033);
#8432=VERTEX_POINT('',#45037);
#8433=VERTEX_POINT('',#45040);
#8434=VERTEX_POINT('',#45044);
#10735=EDGE_CURVE('',#8423,#8423,#6938,.T.);
#10736=EDGE_CURVE('',#8424,#8424,#6939,.T.);
#10737=EDGE_CURVE('',#8424,#8423,#5159,.T.);
#10738=EDGE_CURVE('',#8425,#8425,#6940,.T.);
#10739=EDGE_CURVE('',#8425,#8424,#5160,.T.);
#10740=EDGE_CURVE('',#8426,#8426,#6941,.T.);
#10741=EDGE_CURVE('',#8427,#8427,#6942,.T.);
#10742=EDGE_CURVE('',#8427,#8426,#5161,.T.);
#10743=EDGE_CURVE('',#8428,#8428,#6943,.T.);
#10744=EDGE_CURVE('',#8429,#8429,#6944,.T.);
#10745=EDGE_CURVE('',#8429,#8428,#5162,.T.);
#10746=EDGE_CURVE('',#8430,#8430,#6945,.T.);
#10747=EDGE_CURVE('',#8431,#8431,#6946,.T.);
#10748=EDGE_CURVE('',#8431,#8430,#5163,.T.);
#10749=EDGE_CURVE('',#8432,#8432,#6947,.T.);
#10750=EDGE_CURVE('',#8433,#8433,#6948,.T.);
#10751=EDGE_CURVE('',#8433,#8432,#5164,.T.);
#10752=EDGE_CURVE('',#8434,#8434,#6949,.T.);
#10753=EDGE_CURVE('',#8434,#8433,#5165,.T.);
#15344=ORIENTED_EDGE('',*,*,#10735,.F.);
#15345=ORIENTED_EDGE('',*,*,#10736,.F.);
#15346=ORIENTED_EDGE('',*,*,#10737,.T.);
#15347=ORIENTED_EDGE('',*,*,#10735,.T.);
#15348=ORIENTED_EDGE('',*,*,#10737,.F.);
#15349=ORIENTED_EDGE('',*,*,#10738,.F.);
#15350=ORIENTED_EDGE('',*,*,#10739,.T.);
#15351=ORIENTED_EDGE('',*,*,#10736,.T.);
#15352=ORIENTED_EDGE('',*,*,#10739,.F.);
#15353=ORIENTED_EDGE('',*,*,#10738,.T.);
#15354=ORIENTED_EDGE('',*,*,#10740,.F.);
#15355=ORIENTED_EDGE('',*,*,#10741,.F.);
#15356=ORIENTED_EDGE('',*,*,#10742,.T.);
#15357=ORIENTED_EDGE('',*,*,#10740,.T.);
#15358=ORIENTED_EDGE('',*,*,#10742,.F.);
#15359=ORIENTED_EDGE('',*,*,#10743,.F.);
#15360=ORIENTED_EDGE('',*,*,#10741,.T.);
#15361=ORIENTED_EDGE('',*,*,#10744,.F.);
#15362=ORIENTED_EDGE('',*,*,#10745,.T.);
#15363=ORIENTED_EDGE('',*,*,#10743,.T.);
#15364=ORIENTED_EDGE('',*,*,#10745,.F.);
#15365=ORIENTED_EDGE('',*,*,#10744,.T.);
#15366=ORIENTED_EDGE('',*,*,#10746,.F.);
#15367=ORIENTED_EDGE('',*,*,#10747,.F.);
#15368=ORIENTED_EDGE('',*,*,#10748,.T.);
#15369=ORIENTED_EDGE('',*,*,#10746,.T.);
#15370=ORIENTED_EDGE('',*,*,#10748,.F.);
#15371=ORIENTED_EDGE('',*,*,#10749,.F.);
#15372=ORIENTED_EDGE('',*,*,#10747,.T.);
#15373=ORIENTED_EDGE('',*,*,#10750,.F.);
#15374=ORIENTED_EDGE('',*,*,#10751,.T.);
#15375=ORIENTED_EDGE('',*,*,#10749,.T.);
#15376=ORIENTED_EDGE('',*,*,#10751,.F.);
#15377=ORIENTED_EDGE('',*,*,#10752,.F.);
#15378=ORIENTED_EDGE('',*,*,#10753,.T.);
#15379=ORIENTED_EDGE('',*,*,#10750,.T.);
#15380=ORIENTED_EDGE('',*,*,#10753,.F.);
#15381=ORIENTED_EDGE('',*,*,#10752,.T.);
#15538=CONICAL_SURFACE('',#18031,2.8,0.785398163397448);
#15539=CONICAL_SURFACE('',#18051,2.8,0.785398163397448);
#16480=ADVANCED_FACE('',(#2752),#1541,.T.);
#16481=ADVANCED_FACE('',(#2753),#15538,.T.);
#16482=ADVANCED_FACE('',(#2754),#1805,.T.);
#16483=ADVANCED_FACE('',(#2755,#1055),#1542,.T.);
#16484=ADVANCED_FACE('',(#2756),#1806,.T.);
#16485=ADVANCED_FACE('',(#2757,#1056),#1543,.T.);
#16486=ADVANCED_FACE('',(#2758),#1807,.T.);
#16487=ADVANCED_FACE('',(#2759,#1057),#1544,.T.);
#16488=ADVANCED_FACE('',(#2760),#1808,.T.);
#16489=ADVANCED_FACE('',(#2761,#1058),#1545,.T.);
#16490=ADVANCED_FACE('',(#2762),#1809,.T.);
#16491=ADVANCED_FACE('',(#2763),#15539,.T.);
#16492=ADVANCED_FACE('',(#2764),#1546,.T.);
#16534=CLOSED_SHELL('',(#16480,#16481,#16482,#16483,#16484,#16485,#16486,
#16487,#16488,#16489,#16490,#16491,#16492));
#18028=AXIS2_PLACEMENT_3D('',#45003,#21936,#21937);
#18029=AXIS2_PLACEMENT_3D('',#45004,#21938,#21939);
#18030=AXIS2_PLACEMENT_3D('',#45006,#21940,#21941);
#18031=AXIS2_PLACEMENT_3D('',#45007,#21942,#21943);
#18032=AXIS2_PLACEMENT_3D('',#45009,#21944,#21945);
#18033=AXIS2_PLACEMENT_3D('',#45011,#21947,#21948);
#18034=AXIS2_PLACEMENT_3D('',#45013,#21949,#21950);
#18035=AXIS2_PLACEMENT_3D('',#45015,#21952,#21953);
#18036=AXIS2_PLACEMENT_3D('',#45017,#21954,#21955);
#18037=AXIS2_PLACEMENT_3D('',#45018,#21956,#21957);
#18038=AXIS2_PLACEMENT_3D('',#45020,#21958,#21959);
#18039=AXIS2_PLACEMENT_3D('',#45022,#21961,#21962);
#18040=AXIS2_PLACEMENT_3D('',#45024,#21963,#21964);
#18041=AXIS2_PLACEMENT_3D('',#45025,#21965,#21966);
#18042=AXIS2_PLACEMENT_3D('',#45027,#21967,#21968);
#18043=AXIS2_PLACEMENT_3D('',#45029,#21970,#21971);
#18044=AXIS2_PLACEMENT_3D('',#45031,#21972,#21973);
#18045=AXIS2_PLACEMENT_3D('',#45032,#21974,#21975);
#18046=AXIS2_PLACEMENT_3D('',#45034,#21976,#21977);
#18047=AXIS2_PLACEMENT_3D('',#45036,#21979,#21980);
#18048=AXIS2_PLACEMENT_3D('',#45038,#21981,#21982);
#18049=AXIS2_PLACEMENT_3D('',#45039,#21983,#21984);
#18050=AXIS2_PLACEMENT_3D('',#45041,#21985,#21986);
#18051=AXIS2_PLACEMENT_3D('',#45043,#21988,#21989);
#18052=AXIS2_PLACEMENT_3D('',#45045,#21990,#21991);
#18053=AXIS2_PLACEMENT_3D('',#45047,#21993,#21994);
#21936=DIRECTION('axis',(0.,0.,1.));
#21937=DIRECTION('refdir',(1.,0.,0.));
#21938=DIRECTION('center_axis',(-1.,0.,0.));
#21939=DIRECTION('ref_axis',(0.,0.,1.));
#21940=DIRECTION('center_axis',(1.,0.,0.));
#21941=DIRECTION('ref_axis',(0.,0.,-1.));
#21942=DIRECTION('center_axis',(1.,0.,0.));
#21943=DIRECTION('ref_axis',(0.,1.,0.));
#21944=DIRECTION('center_axis',(1.,0.,0.));
#21945=DIRECTION('ref_axis',(0.,0.,-1.));
#21946=DIRECTION('',(-0.707106781186548,0.707106781186547,8.65956056235493E-17));
#21947=DIRECTION('center_axis',(1.,0.,0.));
#21948=DIRECTION('ref_axis',(0.,1.,0.));
#21949=DIRECTION('center_axis',(1.,0.,0.));
#21950=DIRECTION('ref_axis',(0.,0.,-1.));
#21951=DIRECTION('',(-1.,0.,0.));
#21952=DIRECTION('center_axis',(1.,0.,0.));
#21953=DIRECTION('ref_axis',(0.,0.,-1.));
#21954=DIRECTION('center_axis',(1.,0.,0.));
#21955=DIRECTION('ref_axis',(0.,0.,-1.));
#21956=DIRECTION('center_axis',(1.,0.,0.));
#21957=DIRECTION('ref_axis',(0.,1.,0.));
#21958=DIRECTION('center_axis',(1.,0.,0.));
#21959=DIRECTION('ref_axis',(0.,0.,-1.));
#21960=DIRECTION('',(-1.,0.,0.));
#21961=DIRECTION('center_axis',(-1.,0.,0.));
#21962=DIRECTION('ref_axis',(0.,0.,1.));
#21963=DIRECTION('center_axis',(1.,0.,0.));
#21964=DIRECTION('ref_axis',(0.,0.,-1.));
#21965=DIRECTION('center_axis',(1.,0.,0.));
#21966=DIRECTION('ref_axis',(0.,1.,0.));
#21967=DIRECTION('center_axis',(1.,0.,0.));
#21968=DIRECTION('ref_axis',(0.,0.,-1.));
#21969=DIRECTION('',(-1.,0.,0.));
#21970=DIRECTION('center_axis',(1.,0.,0.));
#21971=DIRECTION('ref_axis',(0.,0.,-1.));
#21972=DIRECTION('center_axis',(1.,0.,0.));
#21973=DIRECTION('ref_axis',(0.,0.,-1.));
#21974=DIRECTION('center_axis',(1.,0.,0.));
#21975=DIRECTION('ref_axis',(0.,1.,0.));
#21976=DIRECTION('center_axis',(1.,0.,0.));
#21977=DIRECTION('ref_axis',(0.,0.,-1.));
#21978=DIRECTION('',(-1.,0.,0.));
#21979=DIRECTION('center_axis',(-1.,0.,0.));
#21980=DIRECTION('ref_axis',(0.,0.,1.));
#21981=DIRECTION('center_axis',(1.,0.,0.));
#21982=DIRECTION('ref_axis',(0.,0.,-1.));
#21983=DIRECTION('center_axis',(1.,0.,0.));
#21984=DIRECTION('ref_axis',(0.,1.,0.));
#21985=DIRECTION('center_axis',(1.,0.,0.));
#21986=DIRECTION('ref_axis',(0.,0.,-1.));
#21987=DIRECTION('',(-1.,0.,0.));
#21988=DIRECTION('center_axis',(-1.,0.,0.));
#21989=DIRECTION('ref_axis',(0.,1.,0.));
#21990=DIRECTION('center_axis',(1.,0.,0.));
#21991=DIRECTION('ref_axis',(0.,0.,-1.));
#21992=DIRECTION('',(-0.707106781186548,-0.707106781186547,-8.65956056235493E-17));
#21993=DIRECTION('center_axis',(1.,0.,0.));
#21994=DIRECTION('ref_axis',(0.,0.,-1.));
#45003=CARTESIAN_POINT('',(0.,0.,0.));
#45004=CARTESIAN_POINT('Origin',(-15.,2.6,0.));
#45005=CARTESIAN_POINT('',(-15.,-2.6,-3.18408167778312E-16));
#45006=CARTESIAN_POINT('Origin',(-15.,0.,0.));
#45007=CARTESIAN_POINT('Origin',(-14.8,0.,0.));
#45008=CARTESIAN_POINT('',(-14.6,-3.,-3.67394039744206E-16));
#45009=CARTESIAN_POINT('Origin',(-14.6,0.,0.));
#45010=CARTESIAN_POINT('',(-14.8,-2.8,-3.42901103761259E-16));
#45011=CARTESIAN_POINT('Origin',(-13.695,0.,0.));
#45012=CARTESIAN_POINT('',(-12.79,-3.,-3.67394039744206E-16));
#45013=CARTESIAN_POINT('Origin',(-12.79,0.,0.));
#45014=CARTESIAN_POINT('',(-13.695,-3.,-3.67394039744206E-16));
#45015=CARTESIAN_POINT('Origin',(-12.79,2.5,0.));
#45016=CARTESIAN_POINT('',(-12.79,-2.5,-3.06161699786838E-16));
#45017=CARTESIAN_POINT('Origin',(-12.79,0.,0.));
#45018=CARTESIAN_POINT('Origin',(-12.42,0.,0.));
#45019=CARTESIAN_POINT('',(-12.05,-2.5,-3.06161699786838E-16));
#45020=CARTESIAN_POINT('Origin',(-12.05,0.,0.));
#45021=CARTESIAN_POINT('',(-12.42,-2.5,-3.06161699786838E-16));
#45022=CARTESIAN_POINT('Origin',(-12.05,3.,0.));
#45023=CARTESIAN_POINT('',(-12.05,-3.,-3.67394039744206E-16));
#45024=CARTESIAN_POINT('Origin',(-12.05,0.,0.));
#45025=CARTESIAN_POINT('Origin',(0.,0.,0.));
#45026=CARTESIAN_POINT('',(12.05,-3.,-3.67394039744206E-16));
#45027=CARTESIAN_POINT('Origin',(12.05,0.,0.));
#45028=CARTESIAN_POINT('',(0.,-3.,-3.67394039744206E-16));
#45029=CARTESIAN_POINT('Origin',(12.05,2.5,0.));
#45030=CARTESIAN_POINT('',(12.05,-2.5,-3.06161699786838E-16));
#45031=CARTESIAN_POINT('Origin',(12.05,0.,0.));
#45032=CARTESIAN_POINT('Origin',(12.42,0.,0.));
#45033=CARTESIAN_POINT('',(12.79,-2.5,-3.06161699786838E-16));
#45034=CARTESIAN_POINT('Origin',(12.79,0.,0.));
#45035=CARTESIAN_POINT('',(12.42,-2.5,-3.06161699786838E-16));
#45036=CARTESIAN_POINT('Origin',(12.79,3.,0.));
#45037=CARTESIAN_POINT('',(12.79,-3.,-3.67394039744206E-16));
#45038=CARTESIAN_POINT('Origin',(12.79,0.,0.));
#45039=CARTESIAN_POINT('Origin',(13.695,0.,0.));
#45040=CARTESIAN_POINT('',(14.6,-3.,-3.67394039744206E-16));
#45041=CARTESIAN_POINT('Origin',(14.6,0.,0.));
#45042=CARTESIAN_POINT('',(13.695,-3.,-3.67394039744206E-16));
#45043=CARTESIAN_POINT('Origin',(14.8,0.,0.));
#45044=CARTESIAN_POINT('',(15.,-2.6,-3.18408167778312E-16));
#45045=CARTESIAN_POINT('Origin',(15.,0.,0.));
#45046=CARTESIAN_POINT('',(14.8,-2.8,-3.42901103761259E-16));
#45047=CARTESIAN_POINT('Origin',(15.,0.,0.));
#45211=UNCERTAINTY_MEASURE_WITH_UNIT(LENGTH_MEASURE(0.01),#45237,
'DISTANCE_ACCURACY_VALUE',
'Maximum model space distance between geometric entities at asserted c
onnectivities');
#45214=UNCERTAINTY_MEASURE_WITH_UNIT(LENGTH_MEASURE(0.01),#45237,
'DISTANCE_ACCURACY_VALUE',
'Maximum model space distance between geometric entities at asserted c
onnectivities');
#45233=(
GEOMETRIC_REPRESENTATION_CONTEXT(3)
GLOBAL_UNCERTAINTY_ASSIGNED_CONTEXT((#45211))
GLOBAL_UNIT_ASSIGNED_CONTEXT((#45237,#45239,#45240))
REPRESENTATION_CONTEXT('','3D')
);
#45236=(
GEOMETRIC_REPRESENTATION_CONTEXT(3)
GLOBAL_UNCERTAINTY_ASSIGNED_CONTEXT((#45214))
GLOBAL_UNIT_ASSIGNED_CONTEXT((#45237,#45239,#45240))
REPRESENTATION_CONTEXT('','3D')
);
#45237=(
LENGTH_UNIT()
NAMED_UNIT(*)
SI_UNIT(.MILLI.,.METRE.)
);
#45239=(
NAMED_UNIT(*)
PLANE_ANGLE_UNIT()
SI_UNIT($,.RADIAN.)
);
#45240=(
NAMED_UNIT(*)
SI_UNIT($,.STERADIAN.)
SOLID_ANGLE_UNIT()
);
#45259=SHAPE_DEFINITION_REPRESENTATION(#45280,#45331);
#45280=PRODUCT_DEFINITION_SHAPE('',$,#45353);
#45331=SHAPE_REPRESENTATION('',(#18028),#45233);
#45334=PRODUCT_DEFINITION_CONTEXT('part definition',#45399,'design');
#45353=PRODUCT_DEFINITION('2026-10-25-23-38-19-947',
'10_Handle_Pin_D6x30',#45374,#45334);
#45374=PRODUCT_DEFINITION_FORMATION('',$,#45419);
#45399=APPLICATION_CONTEXT(
'Core Data for Automotive Mechanical Design Process');
#45400=PRODUCT_CONTEXT('part definition',#45399,'mechanical');
#45419=PRODUCT('2026-10-25-23-38-19-947','10_Handle_Pin_D6x30',$,(#45400));
#45478=COLOUR_RGB('Grey',0.48,0.52,0.57);
#45479=FILL_AREA_STYLE_COLOUR('',#45478);
#45480=FILL_AREA_STYLE('',(#45479));
#45481=SURFACE_STYLE_FILL_AREA(#45480);
#45482=SURFACE_SIDE_STYLE('',(#45481));
#45483=SURFACE_STYLE_USAGE(.BOTH.,#45482);
#45484=PRESENTATION_STYLE_ASSIGNMENT((#45483));
ENDSEC;
END-ISO-10303-21;
